ISO-10303-21;
HEADER;
/* Generated by software containing ST-Developer
 * from STEP Tools, Inc. (www.steptools.com) 
 */

FILE_DESCRIPTION(
/* description */ (''),
/* implementation_level */ '2;1');

FILE_NAME(
/* name */ '13_Dowel_Pin_ISO_8734_8x16.step',
/* time_stamp */ '2026-10-26T06:59:52-07:00',
/* author */ (''),
/* organization */ (''),
/* preprocessor_version */ 'ST-DEVELOPER v20.2',
/* originating_system */ 'Autodesk Translation Framework v15.15.0.0',
/* authorisation */ '');

FILE_SCHEMA (('AUTOMOTIVE_DESIGN { 1 0 10303 214 3 1 1 }'));
ENDSEC;

DATA;
#10=MECHANICAL_DESIGN_GEOMETRIC_PRESENTATION_REPRESENTATION('',(#177),#46395);
#149=SHAPE_REPRESENTATION_RELATIONSHIP('SRR','None',#46469,#163);
#163=ADVANCED_BREP_SHAPE_REPRESENTATION('',(#191),#46394);
#177=STYLED_ITEM('',(#46596),#191);
#191=MANIFOLD_SOLID_BREP('Body1',#24950);
#585=CYLINDRICAL_SURFACE('',#26903,4.);
#1745=PLANE('',#26899);
#1746=PLANE('',#26907);
#3073=FACE_OUTER_BOUND('',#4529,.T.);
#3074=FACE_OUTER_BOUND('',#4530,.T.);
#3075=FACE_OUTER_BOUND('',#4531,.T.);
#3076=FACE_OUTER_BOUND('',#4532,.T.);
#3077=FACE_OUTER_BOUND('',#4533,.T.);
#4529=EDGE_LOOP('',(#23536));
#4530=EDGE_LOOP('',(#23537,#23538,#23539,#23540));
#4531=EDGE_LOOP('',(#23541,#23542,#23543,#23544));
#4532=EDGE_LOOP('',(#23545,#23546,#23547,#23548));
#4533=EDGE_LOOP('',(#23549));
#7400=LINE('',#46329,#10269);
#7401=LINE('',#46333,#10270);
#7402=LINE('',#46337,#10271);
#10269=VECTOR('',#33393,3.8);
#10270=VECTOR('',#33398,4.);
#10271=VECTOR('',#33403,3.8);
#10730=CIRCLE('',#26900,3.6);
#10731=CIRCLE('',#26902,4.);
#10732=CIRCLE('',#26904,4.);
#10733=CIRCLE('',#26906,3.6);
#13013=VERTEX_POINT('',#46324);
#13014=VERTEX_POINT('',#46327);
#13015=VERTEX_POINT('',#46331);
#13016=VERTEX_POINT('',#46335);
#16521=EDGE_CURVE('',#13013,#13013,#10730,.T.);
#16522=EDGE_CURVE('',#13014,#13014,#10731,.T.);
#16523=EDGE_CURVE('',#13014,#13013,#7400,.T.);
#16524=EDGE_CURVE('',#13015,#13015,#10732,.T.);
#16525=EDGE_CURVE('',#13015,#13014,#7401,.T.);
#16526=EDGE_CURVE('',#13016,#13016,#10733,.T.);
#16527=EDGE_CURVE('',#13016,#13015,#7402,.T.);
#23536=ORIENTED_EDGE('',*,*,#16521,.F.);
#23537=ORIENTED_EDGE('',*,*,#16522,.F.);
#23538=ORIENTED_EDGE('',*,*,#16523,.T.);
#23539=ORIENTED_EDGE('',*,*,#16521,.T.);
#23540=ORIENTED_EDGE('',*,*,#16523,.F.);
#23541=ORIENTED_EDGE('',*,*,#16524,.F.);
#23542=ORIENTED_EDGE('',*,*,#16525,.T.);
#23543=ORIENTED_EDGE('',*,*,#16522,.T.);
#23544=ORIENTED_EDGE('',*,*,#16525,.F.);
#23545=ORIENTED_EDGE('',*,*,#16526,.F.);
#23546=ORIENTED_EDGE('',*,*,#16527,.T.);
#23547=ORIENTED_EDGE('',*,*,#16524,.T.);
#23548=ORIENTED_EDGE('',*,*,#16527,.F.);
#23549=ORIENTED_EDGE('',*,*,#16526,.T.);
#23604=CONICAL_SURFACE('',#26901,3.8,0.785398163397449);
#23605=CONICAL_SURFACE('',#26905,3.8,0.785398163397448);
#24932=ADVANCED_FACE('',(#3073),#1745,.T.);
#24933=ADVANCED_FACE('',(#3074),#23604,.T.);
#24934=ADVANCED_FACE('',(#3075),#585,.T.);
#24935=ADVANCED_FACE('',(#3076),#23605,.T.);
#24936=ADVANCED_FACE('',(#3077),#1746,.T.);
#24950=CLOSED_SHELL('',(#24932,#24933,#24934,#24935,#24936));
#26898=AXIS2_PLACEMENT_3D('',#46322,#33383,#33384);
#26899=AXIS2_PLACEMENT_3D('',#46323,#33385,#33386);
#26900=AXIS2_PLACEMENT_3D('',#46325,#33387,#33388);
#26901=AXIS2_PLACEMENT_3D('',#46326,#33389,#33390);
#26902=AXIS2_PLACEMENT_3D('',#46328,#33391,#33392);
#26903=AXIS2_PLACEMENT_3D('',#46330,#33394,#33395);
#26904=AXIS2_PLACEMENT_3D('',#46332,#33396,#33397);
#26905=AXIS2_PLACEMENT_3D('',#46334,#33399,#33400);
#26906=AXIS2_PLACEMENT_3D('',#46336,#33401,#33402);
#26907=AXIS2_PLACEMENT_3D('',#46338,#33404,#33405);
#33383=DIRECTION('axis',(0.,0.,1.));
#33384=DIRECTION('refdir',(1.,0.,0.));
#33385=DIRECTION('center_axis',(-1.,0.,0.));
#33386=DIRECTION('ref_axis',(0.,0.,1.));
#33387=DIRECTION('center_axis',(1.,0.,0.));
#33388=DIRECTION('ref_axis',(0.,0.,-1.));
#33389=DIRECTION('center_axis',(1.,0.,0.));
#33390=DIRECTION('ref_axis',(0.,1.,0.));
#33391=DIRECTION('center_axis',(1.,0.,0.));
#33392=DIRECTION('ref_axis',(0.,0.,-1.));
#33393=DIRECTION('',(-0.707106781186547,0.707106781186548,8.65956056235494E-17));
#33394=DIRECTION('center_axis',(1.,0.,0.));
#33395=DIRECTION('ref_axis',(0.,1.,0.));
#33396=DIRECTION('center_axis',(1.,0.,0.));
#33397=DIRECTION('ref_axis',(0.,0.,-1.));
#33398=DIRECTION('',(-1.,0.,0.));
#33399=DIRECTION('center_axis',(-1.,0.,0.));
#33400=DIRECTION('ref_axis',(0.,1.,0.));
#33401=DIRECTION('center_axis',(1.,0.,0.));
#33402=DIRECTION('ref_axis',(0.,0.,-1.));
#33403=DIRECTION('',(-0.707106781186547,-0.707106781186547,-8.65956056235493E-17));
#33404=DIRECTION('center_axis',(1.,0.,0.));
#33405=DIRECTION('ref_axis',(0.,0.,-1.));
#46322=CARTESIAN_POINT('',(0.,0.,0.));
#46323=CARTESIAN_POINT('Origin',(0.,3.6,0.));
#46324=CARTESIAN_POINT('',(3.46944695195361E-17,-3.6,-4.40872847693047E-16));
#46325=CARTESIAN_POINT('Origin',(0.,0.,0.));
#46326=CARTESIAN_POINT('Origin',(0.2,0.,0.));
#46327=CARTESIAN_POINT('',(0.4,-4.,-4.89858719658941E-16));
#46328=CARTESIAN_POINT('Origin',(0.4,0.,0.));
#46329=CARTESIAN_POINT('',(0.2,-3.8,-4.65365783675994E-16));
#46330=CARTESIAN_POINT('Origin',(8.,0.,0.));
#46331=CARTESIAN_POINT('',(15.6,-4.,-4.89858719658941E-16));
#46332=CARTESIAN_POINT('Origin',(15.6,0.,0.));
#46333=CARTESIAN_POINT('',(8.,-4.,-4.89858719658941E-16));
#46334=CARTESIAN_POINT('Origin',(15.8,0.,0.));
#46335=CARTESIAN_POINT('',(16.,-3.6,-4.40872847693047E-16));
#46336=CARTESIAN_POINT('Origin',(16.,0.,0.));
#46337=CARTESIAN_POINT('',(15.8,-3.8,-4.65365783675994E-16));
#46338=CARTESIAN_POINT('Origin',(16.,0.,0.));
#46378=UNCERTAINTY_MEASURE_WITH_UNIT(LENGTH_MEASURE(0.01),#46396,
'DISTANCE_ACCURACY_VALUE',
'Maximum model space distance between geometric entities at asserted c
onnectivities');
#46379=UNCERTAINTY_MEASURE_WITH_UNIT(LENGTH_MEASURE(0.01),#46396,
'DISTANCE_ACCURACY_VALUE',
'Maximum model space distance between geometric entities at asserted c
onnectivities');
#46394=(
GEOMETRIC_REPRESENTATION_CONTEXT(3)
GLOBAL_UNCERTAINTY_ASSIGNED_CONTEXT((#46378))
GLOBAL_UNIT_ASSIGNED_CONTEXT((#46396,#46398,#46399))
REPRESENTATION_CONTEXT('','3D')
);
#46395=(
GEOMETRIC_REPRESENTATION_CONTEXT(3)
GLOBAL_UNCERTAINTY_ASSIGNED_CONTEXT((#46379))
GLOBAL_UNIT_ASSIGNED_CONTEXT((#46396,#46398,#46399))
REPRESENTATION_CONTEXT('','3D')
);
#46396=(
LENGTH_UNIT()
NAMED_UNIT(*)
SI_UNIT(.MILLI.,.METRE.)
);
#46398=(
NAMED_UNIT(*)
PLANE_ANGLE_UNIT()
SI_UNIT($,.RADIAN.)
);
#46399=(
NAMED_UNIT(*)
SI_UNIT($,.STERADIAN.)
SOLID_ANGLE_UNIT()
);
#46414=SHAPE_DEFINITION_REPRESENTATION(#46429,#46469);
#46429=PRODUCT_DEFINITION_SHAPE('',$,#46485);
#46469=SHAPE_REPRESENTATION('',(#26898),#46394);
#46470=PRODUCT_DEFINITION_CONTEXT('part definition',#46517,'design');
#46485=PRODUCT_DEFINITION('2026-10-26-00-51-19-479',
'13_Dowel_Pin_ISO_8734_8x16',#46500,#46470);
#46500=PRODUCT_DEFINITION_FORMATION('',$,#46533);
#46517=APPLICATION_CONTEXT(
'Core Data for Automotive Mechanical Design Process');
#46518=PRODUCT_CONTEXT('part definition',#46517,'mechanical');
#46533=PRODUCT('2026-10-26-00-51-19-479','13_Dowel_Pin_ISO_8734_8x16',$,
(#46518));
#46590=COLOUR_RGB('Grey',0.48,0.52,0.57);
#46591=FILL_AREA_STYLE_COLOUR('',#46590);
#46592=FILL_AREA_STYLE('',(#46591));
#46593=SURFACE_STYLE_FILL_AREA(#46592);
#46594=SURFACE_SIDE_STYLE('',(#46593));
#46595=SURFACE_STYLE_USAGE(.BOTH.,#46594);
#46596=PRESENTATION_STYLE_ASSIGNMENT((#46595));
ENDSEC;
END-ISO-10303-21;
